ISO-10303-21;
HEADER;
/* Generated by software containing ST-Developer
 * from STEP Tools, Inc. (www.steptools.com) 
 */

FILE_DESCRIPTION(
/* description */ ('Flange-mounted spindle'),
/* implementation_level */ '2;1');

FILE_NAME(
/* name */ 'Hex Nut - M8.step',
/* time_stamp */ '2026-10-27T10:49:51-07:00',
/* author */ (''),
/* organization */ (''),
/* preprocessor_version */ 'ST-DEVELOPER v20.2',
/* originating_system */ 'Autodesk Translation Framework v15.17.0.0',
/* authorisation */ '');

FILE_SCHEMA (('AUTOMOTIVE_DESIGN { 1 0 10303 214 3 1 1 }'));
ENDSEC;

DATA;
#10=MECHANICAL_DESIGN_GEOMETRIC_PRESENTATION_REPRESENTATION('',(#365),#11764);
#11=(
BOUNDED_CURVE()
B_SPLINE_CURVE(2,(#11583,#11584,#11585),.UNSPECIFIED.,.F.,.F.)
B_SPLINE_CURVE_WITH_KNOTS((3,3),(0.14973948338295,0.97160236658079),
 .UNSPECIFIED.)
CURVE()
GEOMETRIC_REPRESENTATION_ITEM()
RATIONAL_B_SPLINE_CURVE((1.07140024848292,1.23714644374248,1.07140024848292))
REPRESENTATION_ITEM('')
);
#12=(
BOUNDED_CURVE()
B_SPLINE_CURVE(2,(#11587,#11588,#11589),.UNSPECIFIED.,.F.,.F.)
B_SPLINE_CURVE_WITH_KNOTS((3,3),(0.14973948338295,0.971602366580789),
 .UNSPECIFIED.)
CURVE()
GEOMETRIC_REPRESENTATION_ITEM()
RATIONAL_B_SPLINE_CURVE((1.07140024848292,1.23714644374248,1.07140024848292))
REPRESENTATION_ITEM('')
);
#13=(
BOUNDED_CURVE()
B_SPLINE_CURVE(2,(#11594,#11595,#11596),.UNSPECIFIED.,.F.,.F.)
B_SPLINE_CURVE_WITH_KNOTS((3,3),(0.14973948338295,0.97160236658079),
 .UNSPECIFIED.)
CURVE()
GEOMETRIC_REPRESENTATION_ITEM()
RATIONAL_B_SPLINE_CURVE((1.07140024848292,1.23714644374248,1.07140024848292))
REPRESENTATION_ITEM('')
);
#14=(
BOUNDED_CURVE()
B_SPLINE_CURVE(2,(#11598,#11599,#11600),.UNSPECIFIED.,.F.,.F.)
B_SPLINE_CURVE_WITH_KNOTS((3,3),(0.14973948338295,0.97160236658079),
 .UNSPECIFIED.)
CURVE()
GEOMETRIC_REPRESENTATION_ITEM()
RATIONAL_B_SPLINE_CURVE((1.07140024848292,1.23714644374248,1.07140024848292))
REPRESENTATION_ITEM('')
);
#15=(
BOUNDED_CURVE()
B_SPLINE_CURVE(2,(#11602,#11603,#11604),.UNSPECIFIED.,.F.,.F.)
B_SPLINE_CURVE_WITH_KNOTS((3,3),(0.14973948338295,0.971602366580789),
 .UNSPECIFIED.)
CURVE()
GEOMETRIC_REPRESENTATION_ITEM()
RATIONAL_B_SPLINE_CURVE((1.07140024848292,1.23714644374248,1.07140024848292))
REPRESENTATION_ITEM('')
);
#16=(
BOUNDED_CURVE()
B_SPLINE_CURVE(2,(#11605,#11606,#11607),.UNSPECIFIED.,.F.,.F.)
B_SPLINE_CURVE_WITH_KNOTS((3,3),(0.14973948338295,0.97160236658079),
 .UNSPECIFIED.)
CURVE()
GEOMETRIC_REPRESENTATION_ITEM()
RATIONAL_B_SPLINE_CURVE((1.07140024848292,1.23714644374248,1.07140024848292))
REPRESENTATION_ITEM('')
);
#17=(
BOUNDED_CURVE()
B_SPLINE_CURVE(2,(#11614,#11615,#11616),.UNSPECIFIED.,.F.,.F.)
B_SPLINE_CURVE_WITH_KNOTS((3,3),(0.14973948338295,0.97160236658079),
 .UNSPECIFIED.)
CURVE()
GEOMETRIC_REPRESENTATION_ITEM()
RATIONAL_B_SPLINE_CURVE((1.07140024848292,1.23714644374248,1.07140024848292))
REPRESENTATION_ITEM('')
);
#18=(
BOUNDED_CURVE()
B_SPLINE_CURVE(2,(#11618,#11619,#11620),.UNSPECIFIED.,.F.,.F.)
B_SPLINE_CURVE_WITH_KNOTS((3,3),(0.14973948338295,0.97160236658079),
 .UNSPECIFIED.)
CURVE()
GEOMETRIC_REPRESENTATION_ITEM()
RATIONAL_B_SPLINE_CURVE((1.07140024848292,1.23714644374248,1.07140024848292))
REPRESENTATION_ITEM('')
);
#19=(
BOUNDED_CURVE()
B_SPLINE_CURVE(2,(#11622,#11623,#11624),.UNSPECIFIED.,.F.,.F.)
B_SPLINE_CURVE_WITH_KNOTS((3,3),(0.14973948338295,0.971602366580789),
 .UNSPECIFIED.)
CURVE()
GEOMETRIC_REPRESENTATION_ITEM()
RATIONAL_B_SPLINE_CURVE((1.07140024848292,1.23714644374248,1.07140024848292))
REPRESENTATION_ITEM('')
);
#20=(
BOUNDED_CURVE()
B_SPLINE_CURVE(2,(#11626,#11627,#11628),.UNSPECIFIED.,.F.,.F.)
B_SPLINE_CURVE_WITH_KNOTS((3,3),(0.14973948338295,0.97160236658079),
 .UNSPECIFIED.)
CURVE()
GEOMETRIC_REPRESENTATION_ITEM()
RATIONAL_B_SPLINE_CURVE((1.07140024848292,1.23714644374248,1.07140024848292))
REPRESENTATION_ITEM('')
);
#21=(
BOUNDED_CURVE()
B_SPLINE_CURVE(2,(#11630,#11631,#11632),.UNSPECIFIED.,.F.,.F.)
B_SPLINE_CURVE_WITH_KNOTS((3,3),(0.14973948338295,0.97160236658079),
 .UNSPECIFIED.)
CURVE()
GEOMETRIC_REPRESENTATION_ITEM()
RATIONAL_B_SPLINE_CURVE((1.07140024848292,1.23714644374248,1.07140024848292))
REPRESENTATION_ITEM('')
);
#22=(
BOUNDED_CURVE()
B_SPLINE_CURVE(2,(#11633,#11634,#11635),.UNSPECIFIED.,.F.,.F.)
B_SPLINE_CURVE_WITH_KNOTS((3,3),(0.14973948338295,0.971602366580789),
 .UNSPECIFIED.)
CURVE()
GEOMETRIC_REPRESENTATION_ITEM()
RATIONAL_B_SPLINE_CURVE((1.07140024848292,1.23714644374248,1.07140024848292))
REPRESENTATION_ITEM('')
);
#276=CONICAL_SURFACE('',#7148,0.734027674973257,1.0471975511966);
#277=CONICAL_SURFACE('',#7150,0.734027674973257,1.0471975511966);
#310=SHAPE_REPRESENTATION_RELATIONSHIP('SRR','None',#11908,#337);
#337=ADVANCED_BREP_SHAPE_REPRESENTATION('',(#390),#11763);
#365=STYLED_ITEM('',(#12106),#390);
#390=MANIFOLD_SOLID_BREP('Body1',#6160);
#504=FACE_BOUND('',#1476,.T.);
#505=FACE_BOUND('',#1478,.T.);
#666=PLANE('',#7152);
#667=PLANE('',#7153);
#668=PLANE('',#7154);
#669=PLANE('',#7158);
#670=PLANE('',#7159);
#671=PLANE('',#7160);
#672=PLANE('',#7161);
#673=PLANE('',#7162);
#1008=FACE_OUTER_BOUND('',#1466,.T.);
#1009=FACE_OUTER_BOUND('',#1467,.T.);
#1010=FACE_OUTER_BOUND('',#1468,.T.);
#1011=FACE_OUTER_BOUND('',#1469,.T.);
#1012=FACE_OUTER_BOUND('',#1470,.T.);
#1013=FACE_OUTER_BOUND('',#1471,.T.);
#1014=FACE_OUTER_BOUND('',#1472,.T.);
#1015=FACE_OUTER_BOUND('',#1473,.T.);
#1016=FACE_OUTER_BOUND('',#1474,.T.);
#1017=FACE_OUTER_BOUND('',#1475,.T.);
#1018=FACE_OUTER_BOUND('',#1477,.T.);
#1466=EDGE_LOOP('',(#5575,#5576,#5577,#5578,#5579,#5580,#5581,#5582,#5583));
#1467=EDGE_LOOP('',(#5584,#5585,#5586,#5587,#5588,#5589,#5590,#5591,#5592));
#1468=EDGE_LOOP('',(#5593,#5594,#5595,#5596));
#1469=EDGE_LOOP('',(#5597,#5598,#5599,#5600));
#1470=EDGE_LOOP('',(#5601,#5602,#5603,#5604));
#1471=EDGE_LOOP('',(#5605,#5606,#5607,#5608));
#1472=EDGE_LOOP('',(#5609,#5610,#5611,#5612));
#1473=EDGE_LOOP('',(#5613,#5614,#5615,#5616));
#1474=EDGE_LOOP('',(#5617,#5618,#5619,#5620));
#1475=EDGE_LOOP('',(#5621));
#1476=EDGE_LOOP('',(#5622));
#1477=EDGE_LOOP('',(#5623));
#1478=EDGE_LOOP('',(#5624));
#1892=LINE('',#11591,#2314);
#1893=LINE('',#11612,#2315);
#1894=LINE('',#11637,#2316);
#1895=LINE('',#11638,#2317);
#1896=LINE('',#11640,#2318);
#1897=LINE('',#11642,#2319);
#1898=LINE('',#11647,#2320);
#1899=LINE('',#11650,#2321);
#1900=LINE('',#11652,#2322);
#2314=VECTOR('',#9001,0.734027674973257);
#2315=VECTOR('',#9008,0.734027674973257);
#2316=VECTOR('',#9011,1.);
#2317=VECTOR('',#9012,1.);
#2318=VECTOR('',#9015,1.);
#2319=VECTOR('',#9018,1.);
#2320=VECTOR('',#9023,0.4);
#2321=VECTOR('',#9028,1.);
#2322=VECTOR('',#9031,1.);
#2645=CIRCLE('',#7149,0.6175);
#2646=CIRCLE('',#7151,0.6175);
#2647=CIRCLE('',#7156,0.338975);
#2648=CIRCLE('',#7157,0.338975);
#3179=VERTEX_POINT('',#11581);
#3180=VERTEX_POINT('',#11582);
#3181=VERTEX_POINT('',#11586);
#3182=VERTEX_POINT('',#11590);
#3183=VERTEX_POINT('',#11593);
#3184=VERTEX_POINT('',#11597);
#3185=VERTEX_POINT('',#11601);
#3186=VERTEX_POINT('',#11609);
#3187=VERTEX_POINT('',#11611);
#3188=VERTEX_POINT('',#11613);
#3189=VERTEX_POINT('',#11617);
#3190=VERTEX_POINT('',#11621);
#3191=VERTEX_POINT('',#11625);
#3192=VERTEX_POINT('',#11629);
#3193=VERTEX_POINT('',#11644);
#3194=VERTEX_POINT('',#11646);
#3980=EDGE_CURVE('',#3179,#3180,#11,.T.);
#3981=EDGE_CURVE('',#3181,#3179,#12,.T.);
#3982=EDGE_CURVE('',#3181,#3182,#1892,.T.);
#3983=EDGE_CURVE('',#3182,#3182,#2645,.T.);
#3984=EDGE_CURVE('',#3183,#3181,#13,.T.);
#3985=EDGE_CURVE('',#3184,#3183,#14,.T.);
#3986=EDGE_CURVE('',#3185,#3184,#15,.T.);
#3987=EDGE_CURVE('',#3180,#3185,#16,.T.);
#3988=EDGE_CURVE('',#3186,#3186,#2646,.T.);
#3989=EDGE_CURVE('',#3186,#3187,#1893,.T.);
#3990=EDGE_CURVE('',#3188,#3187,#17,.T.);
#3991=EDGE_CURVE('',#3189,#3188,#18,.T.);
#3992=EDGE_CURVE('',#3190,#3189,#19,.T.);
#3993=EDGE_CURVE('',#3191,#3190,#20,.T.);
#3994=EDGE_CURVE('',#3192,#3191,#21,.T.);
#3995=EDGE_CURVE('',#3187,#3192,#22,.T.);
#3996=EDGE_CURVE('',#3183,#3192,#1894,.T.);
#3997=EDGE_CURVE('',#3184,#3191,#1895,.T.);
#3998=EDGE_CURVE('',#3181,#3187,#1896,.T.);
#3999=EDGE_CURVE('',#3179,#3188,#1897,.T.);
#4000=EDGE_CURVE('',#3193,#3193,#2647,.F.);
#4001=EDGE_CURVE('',#3193,#3194,#1898,.T.);
#4002=EDGE_CURVE('',#3194,#3194,#2648,.F.);
#4003=EDGE_CURVE('',#3180,#3189,#1899,.T.);
#4004=EDGE_CURVE('',#3185,#3190,#1900,.T.);
#5575=ORIENTED_EDGE('',*,*,#3980,.F.);
#5576=ORIENTED_EDGE('',*,*,#3981,.F.);
#5577=ORIENTED_EDGE('',*,*,#3982,.T.);
#5578=ORIENTED_EDGE('',*,*,#3983,.F.);
#5579=ORIENTED_EDGE('',*,*,#3982,.F.);
#5580=ORIENTED_EDGE('',*,*,#3984,.F.);
#5581=ORIENTED_EDGE('',*,*,#3985,.F.);
#5582=ORIENTED_EDGE('',*,*,#3986,.F.);
#5583=ORIENTED_EDGE('',*,*,#3987,.F.);
#5584=ORIENTED_EDGE('',*,*,#3988,.F.);
#5585=ORIENTED_EDGE('',*,*,#3989,.T.);
#5586=ORIENTED_EDGE('',*,*,#3990,.F.);
#5587=ORIENTED_EDGE('',*,*,#3991,.F.);
#5588=ORIENTED_EDGE('',*,*,#3992,.F.);
#5589=ORIENTED_EDGE('',*,*,#3993,.F.);
#5590=ORIENTED_EDGE('',*,*,#3994,.F.);
#5591=ORIENTED_EDGE('',*,*,#3995,.F.);
#5592=ORIENTED_EDGE('',*,*,#3989,.F.);
#5593=ORIENTED_EDGE('',*,*,#3985,.T.);
#5594=ORIENTED_EDGE('',*,*,#3996,.T.);
#5595=ORIENTED_EDGE('',*,*,#3994,.T.);
#5596=ORIENTED_EDGE('',*,*,#3997,.F.);
#5597=ORIENTED_EDGE('',*,*,#3984,.T.);
#5598=ORIENTED_EDGE('',*,*,#3998,.T.);
#5599=ORIENTED_EDGE('',*,*,#3995,.T.);
#5600=ORIENTED_EDGE('',*,*,#3996,.F.);
#5601=ORIENTED_EDGE('',*,*,#3981,.T.);
#5602=ORIENTED_EDGE('',*,*,#3999,.T.);
#5603=ORIENTED_EDGE('',*,*,#3990,.T.);
#5604=ORIENTED_EDGE('',*,*,#3998,.F.);
#5605=ORIENTED_EDGE('',*,*,#4000,.F.);
#5606=ORIENTED_EDGE('',*,*,#4001,.T.);
#5607=ORIENTED_EDGE('',*,*,#4002,.T.);
#5608=ORIENTED_EDGE('',*,*,#4001,.F.);
#5609=ORIENTED_EDGE('',*,*,#3980,.T.);
#5610=ORIENTED_EDGE('',*,*,#4003,.T.);
#5611=ORIENTED_EDGE('',*,*,#3991,.T.);
#5612=ORIENTED_EDGE('',*,*,#3999,.F.);
#5613=ORIENTED_EDGE('',*,*,#3986,.T.);
#5614=ORIENTED_EDGE('',*,*,#3997,.T.);
#5615=ORIENTED_EDGE('',*,*,#3993,.T.);
#5616=ORIENTED_EDGE('',*,*,#4004,.F.);
#5617=ORIENTED_EDGE('',*,*,#3987,.T.);
#5618=ORIENTED_EDGE('',*,*,#4004,.T.);
#5619=ORIENTED_EDGE('',*,*,#3992,.T.);
#5620=ORIENTED_EDGE('',*,*,#4003,.F.);
#5621=ORIENTED_EDGE('',*,*,#3988,.T.);
#5622=ORIENTED_EDGE('',*,*,#4000,.T.);
#5623=ORIENTED_EDGE('',*,*,#3983,.T.);
#5624=ORIENTED_EDGE('',*,*,#4002,.F.);
#5784=CYLINDRICAL_SURFACE('',#7155,0.338975);
#6119=ADVANCED_FACE('',(#1008),#276,.T.);
#6120=ADVANCED_FACE('',(#1009),#277,.T.);
#6121=ADVANCED_FACE('',(#1010),#666,.T.);
#6122=ADVANCED_FACE('',(#1011),#667,.T.);
#6123=ADVANCED_FACE('',(#1012),#668,.T.);
#6124=ADVANCED_FACE('',(#1013),#5784,.F.);
#6125=ADVANCED_FACE('',(#1014),#669,.T.);
#6126=ADVANCED_FACE('',(#1015),#670,.T.);
#6127=ADVANCED_FACE('',(#1016),#671,.T.);
#6128=ADVANCED_FACE('',(#1017,#504),#672,.T.);
#6129=ADVANCED_FACE('',(#1018,#505),#673,.F.);
#6160=CLOSED_SHELL('',(#6119,#6120,#6121,#6122,#6123,#6124,#6125,#6126,
#6127,#6128,#6129));
#7147=AXIS2_PLACEMENT_3D('',#11579,#8997,#8998);
#7148=AXIS2_PLACEMENT_3D('',#11580,#8999,#9000);
#7149=AXIS2_PLACEMENT_3D('',#11592,#9002,#9003);
#7150=AXIS2_PLACEMENT_3D('',#11608,#9004,#9005);
#7151=AXIS2_PLACEMENT_3D('',#11610,#9006,#9007);
#7152=AXIS2_PLACEMENT_3D('',#11636,#9009,#9010);
#7153=AXIS2_PLACEMENT_3D('',#11639,#9013,#9014);
#7154=AXIS2_PLACEMENT_3D('',#11641,#9016,#9017);
#7155=AXIS2_PLACEMENT_3D('',#11643,#9019,#9020);
#7156=AXIS2_PLACEMENT_3D('',#11645,#9021,#9022);
#7157=AXIS2_PLACEMENT_3D('',#11648,#9024,#9025);
#7158=AXIS2_PLACEMENT_3D('',#11649,#9026,#9027);
#7159=AXIS2_PLACEMENT_3D('',#11651,#9029,#9030);
#7160=AXIS2_PLACEMENT_3D('',#11653,#9032,#9033);
#7161=AXIS2_PLACEMENT_3D('',#11654,#9034,#9035);
#7162=AXIS2_PLACEMENT_3D('',#11655,#9036,#9037);
#8997=DIRECTION('axis',(0.,0.,1.));
#8998=DIRECTION('refdir',(1.,0.,0.));
#8999=DIRECTION('center_axis',(0.,1.,0.));
#9000=DIRECTION('ref_axis',(1.,0.,0.));
#9001=DIRECTION('',(0.866025403784439,-0.5,1.06057523872491E-16));
#9002=DIRECTION('center_axis',(0.,-1.,0.));
#9003=DIRECTION('ref_axis',(1.,0.,0.));
#9004=DIRECTION('center_axis',(0.,-1.,0.));
#9005=DIRECTION('ref_axis',(1.,0.,0.));
#9006=DIRECTION('center_axis',(0.,1.,0.));
#9007=DIRECTION('ref_axis',(1.,0.,0.));
#9008=DIRECTION('',(-0.866025403784439,-0.5,-1.06057523872491E-16));
#9009=DIRECTION('center_axis',(1.4792020664489E-16,0.,-1.));
#9010=DIRECTION('ref_axis',(-1.,0.,-1.4792020664489E-16));
#9011=DIRECTION('',(0.,1.,0.));
#9012=DIRECTION('',(0.,1.,0.));
#9013=DIRECTION('center_axis',(-0.866025403784439,0.,-0.5));
#9014=DIRECTION('ref_axis',(-0.5,0.,0.866025403784439));
#9015=DIRECTION('',(0.,1.,0.));
#9016=DIRECTION('center_axis',(-0.866025403784439,0.,0.5));
#9017=DIRECTION('ref_axis',(0.5,0.,0.866025403784439));
#9018=DIRECTION('',(0.,1.,0.));
#9019=DIRECTION('center_axis',(0.,1.,0.));
#9020=DIRECTION('ref_axis',(1.,0.,0.));
#9021=DIRECTION('center_axis',(0.,1.,0.));
#9022=DIRECTION('ref_axis',(1.,0.,0.));
#9023=DIRECTION('',(0.,-1.,0.));
#9024=DIRECTION('center_axis',(0.,1.,0.));
#9025=DIRECTION('ref_axis',(1.,0.,0.));
#9026=DIRECTION('center_axis',(-2.95840413289779E-16,0.,1.));
#9027=DIRECTION('ref_axis',(1.,0.,2.95840413289779E-16));
#9028=DIRECTION('',(0.,1.,0.));
#9029=DIRECTION('center_axis',(0.866025403784439,0.,-0.5));
#9030=DIRECTION('ref_axis',(-0.5,0.,-0.866025403784439));
#9031=DIRECTION('',(0.,1.,0.));
#9032=DIRECTION('center_axis',(0.866025403784439,0.,0.5));
#9033=DIRECTION('ref_axis',(0.5,0.,-0.866025403784439));
#9034=DIRECTION('center_axis',(0.,1.,0.));
#9035=DIRECTION('ref_axis',(1.,0.,0.));
#9036=DIRECTION('center_axis',(0.,1.,0.));
#9037=DIRECTION('ref_axis',(1.,0.,0.));
#11579=CARTESIAN_POINT('',(0.,0.,0.));
#11580=CARTESIAN_POINT('Origin',(0.,0.067277284513851,0.));
#11581=CARTESIAN_POINT('',(-0.375277674973257,0.0768195421087395,0.65));
#11582=CARTESIAN_POINT('',(0.375277674973257,0.0768195421087395,0.65));
#11583=CARTESIAN_POINT('Ctrl Pts',(-0.375277674973257,0.0768195421087395,
0.65));
#11584=CARTESIAN_POINT('Ctrl Pts',(1.66533453693773E-13,-0.0315137912242439,
0.65));
#11585=CARTESIAN_POINT('Ctrl Pts',(0.375277674973257,0.0768195421087394,
0.65));
#11586=CARTESIAN_POINT('',(-0.750555349946514,0.0768195421087394,-9.19165206894919E-17));
#11587=CARTESIAN_POINT('Ctrl Pts',(-0.750555349946514,0.0768195421087394,
-9.19165206894919E-17));
#11588=CARTESIAN_POINT('Ctrl Pts',(-0.562916512459802,-0.0315137912242434,
0.325000000000144));
#11589=CARTESIAN_POINT('Ctrl Pts',(-0.375277674973257,0.0768195421087395,
0.65));
#11590=CARTESIAN_POINT('',(-0.6175,-2.77555756156289E-17,-7.5621939847349E-17));
#11591=CARTESIAN_POINT('',(-0.734027674973257,0.067277284513851,-8.98924642641573E-17));
#11592=CARTESIAN_POINT('Origin',(0.,0.,0.));
#11593=CARTESIAN_POINT('',(-0.375277674973257,0.0768195421087395,-0.65));
#11594=CARTESIAN_POINT('Ctrl Pts',(-0.375277674973257,0.0768195421087395,
-0.65));
#11595=CARTESIAN_POINT('Ctrl Pts',(-0.562916512459968,-0.0315137912242437,
-0.324999999999856));
#11596=CARTESIAN_POINT('Ctrl Pts',(-0.750555349946514,0.0768195421087395,
-9.19165206894919E-17));
#11597=CARTESIAN_POINT('',(0.375277674973257,0.0768195421087395,-0.65));
#11598=CARTESIAN_POINT('Ctrl Pts',(0.375277674973257,0.0768195421087395,
-0.65));
#11599=CARTESIAN_POINT('Ctrl Pts',(-1.66144875635155E-13,-0.0315137912242437,
-0.65));
#11600=CARTESIAN_POINT('Ctrl Pts',(-0.375277674973257,0.0768195421087395,
-0.65));
#11601=CARTESIAN_POINT('',(0.750555349946514,0.0768195421087394,0.));
#11602=CARTESIAN_POINT('Ctrl Pts',(0.750555349946514,0.0768195421087394,
0.));
#11603=CARTESIAN_POINT('Ctrl Pts',(0.562916512459802,-0.0315137912242436,
-0.325000000000144));
#11604=CARTESIAN_POINT('Ctrl Pts',(0.375277674973257,0.0768195421087395,
-0.65));
#11605=CARTESIAN_POINT('Ctrl Pts',(0.375277674973257,0.0768195421087394,
0.65));
#11606=CARTESIAN_POINT('Ctrl Pts',(0.562916512459968,-0.0315137912242439,
0.324999999999856));
#11607=CARTESIAN_POINT('Ctrl Pts',(0.750555349946514,0.0768195421087394,
0.));
#11608=CARTESIAN_POINT('Origin',(0.,0.612722715486149,0.));
#11609=CARTESIAN_POINT('',(-0.6175,0.68,-7.5621939847349E-17));
#11610=CARTESIAN_POINT('Origin',(0.,0.68,0.));
#11611=CARTESIAN_POINT('',(-0.750555349946514,0.603180457891261,-9.19165206894919E-17));
#11612=CARTESIAN_POINT('',(-0.734027674973257,0.612722715486149,-8.98924642641573E-17));
#11613=CARTESIAN_POINT('',(-0.375277674973257,0.603180457891261,0.65));
#11614=CARTESIAN_POINT('Ctrl Pts',(-0.375277674973257,0.603180457891261,
0.65));
#11615=CARTESIAN_POINT('Ctrl Pts',(-0.562916512459968,0.711513791224243,
0.324999999999856));
#11616=CARTESIAN_POINT('Ctrl Pts',(-0.750555349946514,0.603180457891261,
-9.19165206894919E-17));
#11617=CARTESIAN_POINT('',(0.375277674973257,0.603180457891261,0.65));
#11618=CARTESIAN_POINT('Ctrl Pts',(0.375277674973257,0.603180457891261,
0.65));
#11619=CARTESIAN_POINT('Ctrl Pts',(-1.66755498298699E-13,0.711513791224244,
0.65));
#11620=CARTESIAN_POINT('Ctrl Pts',(-0.375277674973257,0.603180457891261,
0.65));
#11621=CARTESIAN_POINT('',(0.750555349946514,0.603180457891261,0.));
#11622=CARTESIAN_POINT('Ctrl Pts',(0.750555349946514,0.603180457891261,
0.));
#11623=CARTESIAN_POINT('Ctrl Pts',(0.562916512459802,0.711513791224244,
0.325000000000144));
#11624=CARTESIAN_POINT('Ctrl Pts',(0.375277674973257,0.603180457891261,
0.65));
#11625=CARTESIAN_POINT('',(0.375277674973257,0.603180457891261,-0.65));
#11626=CARTESIAN_POINT('Ctrl Pts',(0.375277674973257,0.603180457891261,
-0.65));
#11627=CARTESIAN_POINT('Ctrl Pts',(0.562916512459969,0.711513791224244,
-0.324999999999856));
#11628=CARTESIAN_POINT('Ctrl Pts',(0.750555349946514,0.603180457891261,
0.));
#11629=CARTESIAN_POINT('',(-0.375277674973257,0.603180457891261,-0.65));
#11630=CARTESIAN_POINT('Ctrl Pts',(-0.375277674973257,0.603180457891261,
-0.65));
#11631=CARTESIAN_POINT('Ctrl Pts',(1.66422431391311E-13,0.711513791224244,
-0.65));
#11632=CARTESIAN_POINT('Ctrl Pts',(0.375277674973257,0.603180457891261,
-0.65));
#11633=CARTESIAN_POINT('Ctrl Pts',(-0.750555349946514,0.603180457891261,
-9.19165206894919E-17));
#11634=CARTESIAN_POINT('Ctrl Pts',(-0.562916512459802,0.711513791224244,
-0.325000000000144));
#11635=CARTESIAN_POINT('Ctrl Pts',(-0.375277674973257,0.603180457891261,
-0.65));
#11636=CARTESIAN_POINT('Origin',(0.375277674973257,0.,-0.65));
#11637=CARTESIAN_POINT('',(-0.375277674973257,0.,-0.65));
#11638=CARTESIAN_POINT('',(0.375277674973257,0.,-0.65));
#11639=CARTESIAN_POINT('Origin',(-0.375277674973257,0.,-0.65));
#11640=CARTESIAN_POINT('',(-0.750555349946514,0.,-9.19165206894919E-17));
#11641=CARTESIAN_POINT('Origin',(-0.750555349946514,0.,-9.19165206894919E-17));
#11642=CARTESIAN_POINT('',(-0.375277674973257,0.,0.65));
#11643=CARTESIAN_POINT('Origin',(0.,0.,0.));
#11644=CARTESIAN_POINT('',(-0.338975,0.68,4.15124648740974E-17));
#11645=CARTESIAN_POINT('Origin',(0.,0.68,0.));
#11646=CARTESIAN_POINT('',(-0.338975,0.,4.15124648740974E-17));
#11647=CARTESIAN_POINT('',(-0.338975,0.,4.15124648740974E-17));
#11648=CARTESIAN_POINT('Origin',(0.,0.,0.));
#11649=CARTESIAN_POINT('Origin',(-0.375277674973257,0.,0.65));
#11650=CARTESIAN_POINT('',(0.375277674973257,0.,0.65));
#11651=CARTESIAN_POINT('Origin',(0.750555349946514,0.,0.));
#11652=CARTESIAN_POINT('',(0.750555349946514,0.,0.));
#11653=CARTESIAN_POINT('Origin',(0.375277674973257,0.,0.65));
#11654=CARTESIAN_POINT('Origin',(0.,0.68,-1.11022302462516E-16));
#11655=CARTESIAN_POINT('Origin',(0.,0.,-1.11022302462516E-16));
#11731=UNCERTAINTY_MEASURE_WITH_UNIT(LENGTH_MEASURE(0.001),#11765,
'DISTANCE_ACCURACY_VALUE',
'Maximum model space distance between geometric entities at asserted c
onnectivities');
#11732=UNCERTAINTY_MEASURE_WITH_UNIT(LENGTH_MEASURE(0.001),#11765,
'DISTANCE_ACCURACY_VALUE',
'Maximum model space distance between geometric entities at asserted c
onnectivities');
#11763=(
GEOMETRIC_REPRESENTATION_CONTEXT(3)
GLOBAL_UNCERTAINTY_ASSIGNED_CONTEXT((#11731))
GLOBAL_UNIT_ASSIGNED_CONTEXT((#11765,#11767,#11768))
REPRESENTATION_CONTEXT('','3D')
);
#11764=(
GEOMETRIC_REPRESENTATION_CONTEXT(3)
GLOBAL_UNCERTAINTY_ASSIGNED_CONTEXT((#11732))
GLOBAL_UNIT_ASSIGNED_CONTEXT((#11765,#11767,#11768))
REPRESENTATION_CONTEXT('','3D')
);
#11765=(
LENGTH_UNIT()
NAMED_UNIT(*)
SI_UNIT(.CENTI.,.METRE.)
);
#11767=(
NAMED_UNIT(*)
PLANE_ANGLE_UNIT()
SI_UNIT($,.RADIAN.)
);
#11768=(
NAMED_UNIT(*)
SI_UNIT($,.STERADIAN.)
SOLID_ANGLE_UNIT()
);
#11799=SHAPE_DEFINITION_REPRESENTATION(#11832,#11908);
#11832=PRODUCT_DEFINITION_SHAPE('',$,#11940);
#11908=SHAPE_REPRESENTATION('',(#7147),#11763);
#11909=PRODUCT_DEFINITION_CONTEXT('part definition',#12004,'design');
#11940=PRODUCT_DEFINITION('Hex Nut - M8','Hex Nut - M8',#11971,#11909);
#11971=PRODUCT_DEFINITION_FORMATION('',$,#12036);
#12004=APPLICATION_CONTEXT(
'Core Data for Automotive Mechanical Design Process');
#12005=PRODUCT_CONTEXT('part definition',#12004,'mechanical');
#12036=PRODUCT('Hex Nut - M8','Hex Nut - M8','Hex Nut - M8',(#12005));
#12100=COLOUR_RGB('Black',0.12,0.14,0.17);
#12101=FILL_AREA_STYLE_COLOUR('',#12100);
#12102=FILL_AREA_STYLE('',(#12101));
#12103=SURFACE_STYLE_FILL_AREA(#12102);
#12104=SURFACE_SIDE_STYLE('',(#12103));
#12105=SURFACE_STYLE_USAGE(.BOTH.,#12104);
#12106=PRESENTATION_STYLE_ASSIGNMENT((#12105));
ENDSEC;
END-ISO-10303-21;
